ISO-10303-21;
HEADER;
FILE_DESCRIPTION (('STEP AP203'),
    '1' );
FILE_NAME ('oval head_am_B18.6.7M - M2.5 x 0.45 x 13 Type I Cross Recessed OHMS --13C.step',
    '2026-10-08T23:54:15',
    ( '' ),
    ( '' ),
    'SwSTEP 2.0',
    'SolidWorks 2024',
    '' );
FILE_SCHEMA (( 'AUTOMOTIVE_DESIGN' ));
ENDSEC;

DATA;
#250=DIRECTION ( 'NONE',  ( -1.000000000000000000, 0.000000000000000000, 0.000000000000000000 ) ) ;
#473=DIRECTION ( 'NONE',  ( -1.000000000000000000, -0.000000000000000000, -0.000000000000000000 ) ) ;
#715=CARTESIAN_POINT ( 'NONE',  ( 1.949999999999999956, -0.1925000000000007261, 0.1924999999999992828 ) ) ;
#1017=ORIENTED_EDGE ( 'NONE', *, *, #45920, .T. ) ;
#1324=VECTOR ( 'NONE', #23142, 999.9999999999998863 ) ;
#1353=CARTESIAN_POINT ( 'NONE',  ( 13.60020833695035947, 0.000000000000000000, 0.000000000000000000 ) ) ;
#1506=CLOSED_SHELL ( 'NONE', ( #10304, #65184, #24838, #77619, #76239, #98548, #93754, #19318, #8575, #41539, #53116, #38460, #95025, #44284, #21171, #57020, #74206, #28690, #45159, #28308, #38824, #28481 ) ) ;
#1533=CARTESIAN_POINT ( 'NONE',  ( 0.000000000000000000, 0.000000000000000000, 0.000000000000000000 ) ) ;
#1738=ORIENTED_EDGE ( 'NONE', *, *, #3191, .F. ) ;
#1863=CARTESIAN_POINT ( 'NONE',  ( 0.1645010273463760886, 1.417169167140627906, 0.3687607960183699740 ) ) ;
#1937=DIRECTION ( 'NONE',  ( -1.000000000000000000, -0.000000000000000000, -0.000000000000000000 ) ) ;
#2280=ORIENTED_EDGE ( 'NONE', *, *, #20402, .T. ) ;
#2717=AXIS2_PLACEMENT_3D ( 'NONE', #61487, #45256, #8190 ) ;
#3144=AXIS2_PLACEMENT_3D ( 'NONE', #58903, #43673, #74611 ) ;
#3191=EDGE_CURVE ( 'NONE', #76987, #54552, #68384, .T. ) ;
#3324=ORIENTED_EDGE ( 'NONE', *, *, #76805, .F. ) ;
#3574=PLANE ( 'NONE',  #93555 ) ;
#3602=PRODUCT_DEFINITION ( 'UNKNOWN', '', #79677, #99657 ) ;
#4015=LINE ( 'NONE', #65438, #4459 ) ;
#4050=PLANE ( 'NONE',  #81309 ) ;
#4108=AXIS2_PLACEMENT_3D ( 'NONE', #51961, #22472, #30101 ) ;
#4203=VERTEX_POINT ( 'NONE', #88617 ) ;
#4358=DIRECTION ( 'NONE',  ( -0.8246584009594635223, 0.5656310827093757876, 0.000000000000000000 ) ) ;
#4360=AXIS2_PLACEMENT_3D ( 'NONE', #48752, #86789, #47742 ) ;
#4459=VECTOR ( 'NONE', #50190, 1000.000000000000114 ) ;
#4551=VERTEX_POINT ( 'NONE', #7113 ) ;
#4701=CARTESIAN_POINT ( 'NONE',  ( 0.1645010273463760886, 0.3687607960183654776, 1.417169167140628794 ) ) ;
#4757=VERTEX_POINT ( 'NONE', #31957 ) ;
#4865=CARTESIAN_POINT ( 'NONE',  ( 2.230654205607476293, -6.505213034913026604E-16, -0.1647943925233646134 ) ) ;
#4872=ORIENTED_EDGE ( 'NONE', *, *, #71817, .F. ) ;
#4981=CARTESIAN_POINT ( 'NONE',  ( 0.1645010273463760886, -1.417169167140626573, 0.3687607960183696965 ) ) ;
#5411=VERTEX_POINT ( 'NONE', #42359 ) ;
#5451=FACE_OUTER_BOUND ( 'NONE', #48159, .T. ) ;
#5538=FACE_OUTER_BOUND ( 'NONE', #8765, .T. ) ;
#5881=DIRECTION ( 'NONE',  ( -0.8246584009594636333, 0.5656310827093757876, 0.000000000000000000 ) ) ;
#6042=DIRECTION ( 'NONE',  ( 0.8219392559241306406, 0.08114015731558892053, -0.5637660281018073150 ) ) ;
#6162=CARTESIAN_POINT ( 'NONE',  ( 0.4325450954222598288, 0.000000000000000000, 2.350000000000000089 ) ) ;
#6242=CONICAL_SURFACE ( 'NONE', #84040, 1.249999999999996003, 0.7853981633974514986 ) ;
#6295=DIRECTION ( 'NONE',  ( -0.09824042138329590335, 0.9951627101165078093, 3.519298150595267489E-15 ) ) ;
#6407=DIRECTION ( 'NONE',  ( 0.000000000000000000, 0.000000000000000000, 1.000000000000000000 ) ) ;
#6660=AXIS2_PLACEMENT_3D ( 'NONE', #92543, #9301, #47885 ) ;
#6786=DIRECTION ( 'NONE',  ( -0.9951627101165076983, -0.09824042138329588947, -3.430045979798635096E-16 ) ) ;
#6927=LINE ( 'NONE', #61236, #47217 ) ;
#6930=DIRECTION ( 'NONE',  ( -0.8246584009594636333, 0.000000000000000000, -0.5656310827093756766 ) ) ;
#6938=LINE ( 'NONE', #92664, #1324 ) ;
#7113=CARTESIAN_POINT ( 'NONE',  ( 0.02224039135773590858, 0.3828044741864786715, 0.3828044741864790046 ) ) ;
#7159=CARTESIAN_POINT ( 'NONE',  ( 2.246611357655420083, 0.1632191352058106337, 0.1632191352058112166 ) ) ;
#7454=CARTESIAN_POINT ( 'NONE',  ( 0.1645010273463769490, -1.417169167140626129, -0.3687607960183705291 ) ) ;
#7823=FACE_OUTER_BOUND ( 'NONE', #57908, .T. ) ;
#7922=FACE_OUTER_BOUND ( 'NONE', #13229, .T. ) ;
#8089=CARTESIAN_POINT ( 'NONE',  ( -15.87499999999997868, 0.000000000000000000, 1.249999999999997558 ) ) ;
#8190=DIRECTION ( 'NONE',  ( 0.000000000000000000, 0.000000000000000000, 1.000000000000000000 ) ) ;
#8215=ORIENTED_EDGE ( 'NONE', *, *, #93039, .F. ) ;
#8248=ORIENTED_EDGE ( 'NONE', *, *, #44167, .F. ) ;
#8518=CIRCLE ( 'NONE', #94411, 6.119803529381341534 ) ;
#8575=ADVANCED_FACE ( 'NONE', ( #88793 ), #4050, .T. ) ;
#8669=VECTOR ( 'NONE', #52970, 1000.000000000000000 ) ;
#8765=EDGE_LOOP ( 'NONE', ( #17119, #26129, #90646, #35347 ) ) ;
#8857=VECTOR ( 'NONE', #68010, 1000.000000000000000 ) ;
#8875=EDGE_CURVE ( 'NONE', #57442, #78612, #82957, .T. ) ;
#8952=PLANE ( 'NONE',  #71875 ) ;
#9185=AXIS2_PLACEMENT_3D ( 'NONE', #41219, #95997, #11751 ) ;
#9194=FACE_OUTER_BOUND ( 'NONE', #49472, .T. ) ;
#9195=CARTESIAN_POINT ( 'NONE',  ( 13.60020833695035947, 1.530808498934190338E-16, -1.249999999999998890 ) ) ;
#9301=DIRECTION ( 'NONE',  ( -0.09824042138329623641, -0.9951627101165078093, -3.504396110891626425E-15 ) ) ;
#9810=ORIENTED_EDGE ( 'NONE', *, *, #13134, .T. ) ;
#9837=ORIENTED_EDGE ( 'NONE', *, *, #98676, .T. ) ;
#9944=DIRECTION ( 'NONE',  ( -0.7071067811865452413, 8.659560562354961208E-17, -0.7071067811865497932 ) ) ;
#9962=DIRECTION ( 'NONE',  ( 0.5656310827093757876, -0.8246584009594636333, -1.161164194647627127E-16 ) ) ;
#10159=DIRECTION ( 'NONE',  ( -0.09824042138329590335, 4.470611911092166224E-17, -0.9951627101165078093 ) ) ;
#10201=CIRCLE ( 'NONE', #66930, 6.600000000000001421 ) ;
#10285=ORIENTED_EDGE ( 'NONE', *, *, #29767, .T. ) ;
#10304=ADVANCED_FACE ( 'NONE', ( #49267 ), #93908, .T. ) ;
#10382=EDGE_CURVE ( 'NONE', #91571, #78143, #8518, .T. ) ;
#10458=CARTESIAN_POINT ( 'NONE',  ( 1.949999999999999956, -0.1925000000000001155, -0.1925000000000000600 ) ) ;
#10517=ORIENTED_EDGE ( 'NONE', *, *, #29709, .F. ) ;
#10726=DIRECTION ( 'NONE',  ( -0.9951627101165076983, 0.000000000000000000, 0.09824042138329588947 ) ) ;
#11183=ORIENTED_EDGE ( 'NONE', *, *, #49168, .T. ) ;
#11386=VERTEX_POINT ( 'NONE', #4701 ) ;
#11525=ORIENTED_EDGE ( 'NONE', *, *, #70001, .F. ) ;
#11662=FACE_OUTER_BOUND ( 'NONE', #66953, .T. ) ;
#11725=CIRCLE ( 'NONE', #68457, 6.594667762285749468 ) ;
#11751=DIRECTION ( 'NONE',  ( 0.000000000000000000, 0.000000000000000000, 1.000000000000000000 ) ) ;
#11849=AXIS2_PLACEMENT_3D ( 'NONE', #18564, #28184, #4358 ) ;
#12070=CARTESIAN_POINT ( 'NONE',  ( 0.4325450954222598288, 2.349999999999997868, 2.877919977996277362E-16 ) ) ;
#12093=DIRECTION ( 'NONE',  ( 0.9951627101165076983, -0.09824042138329622254, 0.000000000000000000 ) ) ;
#12231=DIRECTION ( 'NONE',  ( -0.09824042138329623641, -2.980407940728110405E-17, 0.9951627101165078093 ) ) ;
#12240=FACE_OUTER_BOUND ( 'NONE', #13497, .T. ) ;
#12679=DIRECTION ( 'NONE',  ( -0.5656310827093757876, -0.8246584009594636333, -1.161164194647626387E-16 ) ) ;
#12976=CARTESIAN_POINT ( 'NONE',  ( 5.202077965628057576, 7.402934475628871785E-15, -2.038091937962834166 ) ) ;
#13134=EDGE_CURVE ( 'NONE', #5411, #62723, #23806, .T. ) ;
#13229=EDGE_LOOP ( 'NONE', ( #41343, #10517, #36071 ) ) ;
#13269=DIRECTION ( 'NONE',  ( -0.9903949459893287566, 0.09776975748868974025, 0.09776975748868974025 ) ) ;
#13459=PLANE ( 'NONE',  #43837 ) ;
#13497=EDGE_LOOP ( 'NONE', ( #40420, #39537, #96387, #61781, #45947 ) ) ;
#13540=MECHANICAL_CONTEXT ( 'NONE', #39445, 'mechanical' ) ;
#14068=AXIS2_PLACEMENT_3D ( 'NONE', #75902, #28745, #6407 ) ;
#14201=CARTESIAN_POINT ( 'NONE',  ( -15.87499999999997868, 0.000000000000000000, 2.349999999999999645 ) ) ;
#14342=EDGE_CURVE ( 'NONE', #74207, #57442, #59395, .T. ) ;
#14634=VECTOR ( 'NONE', #6042, 1000.000000000000227 ) ;
#15180=EDGE_CURVE ( 'NONE', #74207, #20296, #28412, .T. ) ;
#15253=ORIENTED_EDGE ( 'NONE', *, *, #85300, .T. ) ;
#15285=DIRECTION ( 'NONE',  ( 0.8219392559241306406, -0.5637660281018075370, 0.08114015731558719968 ) ) ;
#15404=DIRECTION ( 'NONE',  ( -0.9951627101165078093, 1.776356839400250267E-15, 0.09824042138329590335 ) ) ;
#15447=DIRECTION ( 'NONE',  ( 0.8219392559241307517, -0.08114015731558921196, 0.5637660281018073150 ) ) ;
#15468=CARTESIAN_POINT ( 'NONE',  ( 6.600000000000001421, 0.000000000000000000, 0.000000000000000000 ) ) ;
#15730=AXIS2_PLACEMENT_3D ( 'NONE', #49301, #80230, #10726 ) ;
#15788=ORIENTED_EDGE ( 'NONE', *, *, #20794, .T. ) ;
#15860=ORIENTED_EDGE ( 'NONE', *, *, #18647, .F. ) ;
#15886=ORIENTED_EDGE ( 'NONE', *, *, #65178, .T. ) ;
#15903=ORIENTED_EDGE ( 'NONE', *, *, #21288, .F. ) ;
#15989=VERTEX_POINT ( 'NONE', #43169 ) ;
#16222=ORIENTED_EDGE ( 'NONE', *, *, #8875, .T. ) ;
#16549=FACE_OUTER_BOUND ( 'NONE', #63698, .T. ) ;
#16569=DIRECTION ( 'NONE',  ( 0.000000000000000000, 0.000000000000000000, 1.000000000000000000 ) ) ;
#16787=VERTEX_POINT ( 'NONE', #48038 ) ;
#17033=PLANE ( 'NONE',  #75727 ) ;
#17060=DIRECTION ( 'NONE',  ( -0.000000000000000000, 0.000000000000000000, 1.000000000000000000 ) ) ;
#17077=DIRECTION ( 'NONE',  ( 0.9951627101165076983, -0.09824042138329622254, -8.881784197001249168E-15 ) ) ;
#17119=ORIENTED_EDGE ( 'NONE', *, *, #55862, .F. ) ;
#17333=ORIENTED_EDGE ( 'NONE', *, *, #76562, .F. ) ;
#17339=EDGE_CURVE ( 'NONE', #62723, #74207, #42686, .T. ) ;
#17556=CARTESIAN_POINT ( 'NONE',  ( 1.000208336950358934, 0.000000000000000000, 0.000000000000000000 ) ) ;
#17578=EDGE_CURVE ( 'NONE', #4203, #57442, #69047, .T. ) ;
#17600=ORIENTED_EDGE ( 'NONE', *, *, #84067, .F. ) ;
#17687=CIRCLE ( 'NONE', #97063, 1.249999999999999112 ) ;
#18138=ORIENTED_EDGE ( 'NONE', *, *, #45920, .F. ) ;
#18333=PLANE ( 'NONE',  #15730 ) ;
#18564=CARTESIAN_POINT ( 'NONE',  ( 5.202077965628057576, -2.038091937962834166, -2.869745073849994963E-16 ) ) ;
#18576=ORIENTED_EDGE ( 'NONE', *, *, #30402, .T. ) ;
#18647=EDGE_CURVE ( 'NONE', #62723, #95252, #51304, .T. ) ;
#19318=ADVANCED_FACE ( 'NONE', ( #87849 ), #18333, .T. ) ;
#19594=DIRECTION ( 'NONE',  ( -0.5656310827093757876, 2.995395837334947896E-15, -0.8246584009594636333 ) ) ;
#19705=EDGE_LOOP ( 'NONE', ( #8248, #20962, #70094, #70931, #31327, #79635, #9837, #77027, #15886, #20731, #42309 ) ) ;
#20296=VERTEX_POINT ( 'NONE', #32689 ) ;
#20340=PLANE ( 'NONE',  #50280 ) ;
#20373=ORIENTED_EDGE ( 'NONE', *, *, #65521, .F. ) ;
#20402=EDGE_CURVE ( 'NONE', #78762, #53932, #30289, .T. ) ;
#20520=CARTESIAN_POINT ( 'NONE',  ( 6.573941812937369455, 0.2639660507643281639, 9.334907998774166978E-16 ) ) ;
#20554=UNCERTAINTY_MEASURE_WITH_UNIT (LENGTH_MEASURE( 1.000000000000000082E-05 ), #50131, 'distance_accuracy_value', 'NONE');
#20731=ORIENTED_EDGE ( 'NONE', *, *, #65957, .T. ) ;
#20794=EDGE_CURVE ( 'NONE', #78762, #76987, #4015, .T. ) ;
#20923=CARTESIAN_POINT ( 'NONE',  ( 2.100208336950355914, 2.204364238465233111E-16, -1.249999999999996003 ) ) ;
#20962=ORIENTED_EDGE ( 'NONE', *, *, #96566, .T. ) ;
#21079=CIRCLE ( 'NONE', #26011, 6.594667762285749468 ) ;
#21171=ADVANCED_FACE ( 'NONE', ( #52566 ), #43951, .F. ) ;
#21288=EDGE_CURVE ( 'NONE', #15989, #98229, #53054, .T. ) ;
#21395=VECTOR ( 'NONE', #9944, 1000.000000000000000 ) ;
#21594=EDGE_LOOP ( 'NONE', ( #98640, #53409, #17333 ) ) ;
#21749=DIRECTION ( 'NONE',  ( 0.000000000000000000, 0.000000000000000000, 1.000000000000000000 ) ) ;
#22022=AXIS2_PLACEMENT_3D ( 'NONE', #99923, #30434, #71514 ) ;
#22064=DIRECTION ( 'NONE',  ( 0.9951627101165076983, 0.000000000000000000, 0.09824042138329622254 ) ) ;
#22472=DIRECTION ( 'NONE',  ( -1.000000000000000000, -0.000000000000000000, -0.000000000000000000 ) ) ;
#22493=DIRECTION ( 'NONE',  ( -0.5656310827093756766, 0.8246584009594636333, 1.161164194647626880E-16 ) ) ;
#23118=AXIS2_PLACEMENT_3D ( 'NONE', #80194, #47751, #71088 ) ;
#23126=DIRECTION ( 'NONE',  ( 0.000000000000000000, 0.000000000000000000, 1.000000000000000000 ) ) ;
#23142=DIRECTION ( 'NONE',  ( 0.8219392559241307517, 0.08114015731558495148, 0.5637660281018078701 ) ) ;
#23151=SPHERICAL_SURFACE ( 'NONE', #63695, 6.600000000000001421 ) ;
#23479=CARTESIAN_POINT ( 'NONE',  ( -15.87499999999997868, 1.530808498934188612E-16, -1.249999999999997558 ) ) ;
#23547=VERTEX_POINT ( 'NONE', #45312 ) ;
#23679=CARTESIAN_POINT ( 'NONE',  ( 6.573941812937369455, -0.2639660507643297183, -9.295380466955404257E-16 ) ) ;
#23748=DIRECTION ( 'NONE',  ( 0.000000000000000000, 0.000000000000000000, 1.000000000000000000 ) ) ;
#23806=LINE ( 'NONE', #8089, #31641 ) ;
#24135=CIRCLE ( 'NONE', #58208, 6.594667762285751245 ) ;
#24157=SHAPE_DEFINITION_REPRESENTATION ( #80619, #32845 ) ;
#24379=CARTESIAN_POINT ( 'NONE',  ( -15.87499999999997868, 2.877919977996279334E-16, -2.349999999999999645 ) ) ;
#24838=ADVANCED_FACE ( 'NONE', ( #12240 ), #58451, .T. ) ;
#24854=DIRECTION ( 'NONE',  ( 1.000000000000000000, 0.000000000000000000, 0.000000000000000000 ) ) ;
#24885=VECTOR ( 'NONE', #68884, 1000.000000000000000 ) ;
#25018=CARTESIAN_POINT ( 'NONE',  ( 1.949999999999999956, 0.1925000000000007538, -0.1924999999999994493 ) ) ;
#25268=DIRECTION ( 'NONE',  ( -1.000000000000000000, -0.000000000000000000, -0.000000000000000000 ) ) ;
#25433=DIRECTION ( 'NONE',  ( -0.9903949459893287566, -0.09776975748868939331, -0.09776975748869010108 ) ) ;
#25636=EDGE_CURVE ( 'NONE', #95664, #23547, #60588, .T. ) ;
#26011=AXIS2_PLACEMENT_3D ( 'NONE', #32684, #79856, #96098 ) ;
#26094=DIRECTION ( 'NONE',  ( 0.09824042138329625029, 2.980407940728111021E-17, -0.9951627101165079203 ) ) ;
#26129=ORIENTED_EDGE ( 'NONE', *, *, #84145, .T. ) ;
#26288=( NAMED_UNIT ( * ) PLANE_ANGLE_UNIT ( ) SI_UNIT ( $, .RADIAN. ) );
#26335=DIRECTION ( 'NONE',  ( 0.09824042138329625029, 0.9951627101165079203, 3.504396110891627214E-15 ) ) ;
#26483=ORIENTED_EDGE ( 'NONE', *, *, #44779, .T. ) ;
#27176=DIRECTION ( 'NONE',  ( 0.000000000000000000, 0.000000000000000000, 1.000000000000000000 ) ) ;
#27534=CIRCLE ( 'NONE', #40499, 6.594667762285751245 ) ;
#27913=CARTESIAN_POINT ( 'NONE',  ( 2.246611357655420083, -0.1632191352058117717, 0.1632191352058111888 ) ) ;
#27937=EDGE_LOOP ( 'NONE', ( #15788, #48826, #8215 ) ) ;
#28012=EDGE_CURVE ( 'NONE', #53932, #98229, #49783, .T. ) ;
#28184=DIRECTION ( 'NONE',  ( -0.5656310827093757876, -0.8246584009594636333, -1.161164194647626387E-16 ) ) ;
#28223=CARTESIAN_POINT ( 'NONE',  ( 2.246611357655420083, 0.1632191352058117717, -0.1632191352058112166 ) ) ;
#28308=ADVANCED_FACE ( 'NONE', ( #71080 ), #39616, .T. ) ;
#28393=CARTESIAN_POINT ( 'NONE',  ( 13.60020833695035947, 0.000000000000000000, 0.000000000000000000 ) ) ;
#28412=CIRCLE ( 'NONE', #60815, 2.349999999999999645 ) ;
#28481=ADVANCED_FACE ( 'NONE', ( #11662 ), #3574, .F. ) ;
#28690=ADVANCED_FACE ( 'NONE', ( #7922 ), #17033, .T. ) ;
#28739=ORIENTED_EDGE ( 'NONE', *, *, #13134, .F. ) ;
#28745=DIRECTION ( 'NONE',  ( -1.000000000000000000, -0.000000000000000000, -0.000000000000000000 ) ) ;
#29016=ORIENTED_EDGE ( 'NONE', *, *, #17578, .F. ) ;
#29029=CARTESIAN_POINT ( 'NONE',  ( 6.600000000000001421, 0.000000000000000000, 0.000000000000000000 ) ) ;
#29044=CIRCLE ( 'NONE', #42047, 6.119803529381341534 ) ;
#29112=CARTESIAN_POINT ( 'NONE',  ( 0.000000000000000000, 1.530000000000000027, 0.3849999999999992872 ) ) ;
#29709=EDGE_CURVE ( 'NONE', #15989, #64340, #66509, .T. ) ;
#29720=DIRECTION ( 'NONE',  ( 0.5656310827093757876, 0.8246584009594636333, 1.161164194647626634E-16 ) ) ;
#29767=EDGE_CURVE ( 'NONE', #95664, #56245, #30176, .T. ) ;
#29811=CARTESIAN_POINT ( 'NONE',  ( 1.949999999999999956, -0.1925000000000001155, -0.1925000000000000600 ) ) ;
#30101=DIRECTION ( 'NONE',  ( 0.000000000000000000, 0.000000000000000000, 1.000000000000000000 ) ) ;
#30176=CIRCLE ( 'NONE', #66084, 6.119803529381342422 ) ;
#30289=CIRCLE ( 'NONE', #46608, 6.119803529381341534 ) ;
#30297=CIRCLE ( 'NONE', #14068, 2.350000000000000089 ) ;
#30402=EDGE_CURVE ( 'NONE', #98229, #64340, #6927, .T. ) ;
#30434=DIRECTION ( 'NONE',  ( -1.000000000000000000, -0.000000000000000000, -0.000000000000000000 ) ) ;
#30873=ORIENTED_EDGE ( 'NONE', *, *, #28012, .F. ) ;
#31023=VERTEX_POINT ( 'NONE', #91413 ) ;
#31162=DIRECTION ( 'NONE',  ( -0.8246584009594636333, -1.974890369949422540E-15, 0.5656310827093757876 ) ) ;
#31303=FACE_OUTER_BOUND ( 'NONE', #66300, .T. ) ;
#31327=ORIENTED_EDGE ( 'NONE', *, *, #20402, .F. ) ;
#31641=VECTOR ( 'NONE', #473, 1000.000000000000000 ) ;
#31664=DIRECTION ( 'NONE',  ( 0.5656310827093757876, -2.995395837334947501E-15, 0.8246584009594636333 ) ) ;
#31815=ORIENTED_EDGE ( 'NONE', *, *, #51290, .F. ) ;
#31957=CARTESIAN_POINT ( 'NONE',  ( 0.02224039135773677595, -0.3828044741864776723, -0.3828044741864797262 ) ) ;
#32288=DIRECTION ( 'NONE',  ( -1.000000000000000000, 0.000000000000000000, -0.000000000000000000 ) ) ;
#32684=CARTESIAN_POINT ( 'NONE',  ( 6.573941812937369455, 0.2639660507643281639, 9.334907998774166978E-16 ) ) ;
#32689=CARTESIAN_POINT ( 'NONE',  ( 1.000208336950358934, 2.877919977996279334E-16, -2.349999999999999645 ) ) ;
#32808=CARTESIAN_POINT ( 'NONE',  ( 2.100208336950355914, 0.000000000000000000, 0.000000000000000000 ) ) ;
#32845=SHAPE_REPRESENTATION ( 'oval head_am_B18.6.7M - M2.5 x 0.45 x 13 Type I Cross Recessed OHMS --13C', ( #37391 ), #82851 ) ;
#33139=VECTOR ( 'NONE', #73412, 1000.000000000000114 ) ;
#33360=VECTOR ( 'NONE', #57528, 1000.000000000000000 ) ;
#33662=CARTESIAN_POINT ( 'NONE',  ( 6.600000000000001421, 0.000000000000000000, 0.000000000000000000 ) ) ;
#35024=DIRECTION ( 'NONE',  ( -0.5656310827093756766, -2.995395837334948290E-15, 0.8246584009594636333 ) ) ;
#35035=CARTESIAN_POINT ( 'NONE',  ( 1.949999999999999956, -0.1925000000000001155, -0.1925000000000000600 ) ) ;
#35347=ORIENTED_EDGE ( 'NONE', *, *, #45604, .F. ) ;
#36034=CARTESIAN_POINT ( 'NONE',  ( 0.1553305729023591875, 1.423459158329793306, 1.743234701965566823E-16 ) ) ;
#36071=ORIENTED_EDGE ( 'NONE', *, *, #42483, .F. ) ;
#36488=DIRECTION ( 'NONE',  ( -1.000000000000000000, -0.000000000000000000, -0.000000000000000000 ) ) ;
#36679=AXIS2_PLACEMENT_3D ( 'NONE', #10458, #9962, #49042 ) ;
#37060=EDGE_LOOP ( 'NONE', ( #44732, #84881, #72538 ) ) ;
#37193=ORIENTED_EDGE ( 'NONE', *, *, #65521, .T. ) ;
#37391=AXIS2_PLACEMENT_3D ( 'NONE', #1533, #63447, #24854 ) ;
#37512=DIRECTION ( 'NONE',  ( -1.000000000000000000, -0.000000000000000000, -0.000000000000000000 ) ) ;
#37831=CARTESIAN_POINT ( 'NONE',  ( 6.573941812937369455, 1.185825954564562440E-17, -0.2639660507643281639 ) ) ;
#37881=DIRECTION ( 'NONE',  ( 0.8219392559241307517, 0.5637660281018075370, -0.08114015731558690825 ) ) ;
#37986=DIRECTION ( 'NONE',  ( -0.9951627101165076983, 0.000000000000000000, 0.09824042138329588947 ) ) ;
#38394=DIRECTION ( 'NONE',  ( 0.000000000000000000, -1.000000000000000000, 0.000000000000000000 ) ) ;
#38460=ADVANCED_FACE ( 'NONE', ( #5538 ), #92860, .T. ) ;
#38488=CARTESIAN_POINT ( 'NONE',  ( 0.4325450954222598288, 0.000000000000000000, 0.000000000000000000 ) ) ;
#38641=DIRECTION ( 'NONE',  ( 0.000000000000000000, 0.000000000000000000, 1.000000000000000000 ) ) ;
#38824=ADVANCED_FACE ( 'NONE', ( #81559 ), #75797, .T. ) ;
#39231=DIRECTION ( 'NONE',  ( 0.8246584009594635223, 0.5656310827093757876, 0.000000000000000000 ) ) ;
#39445=APPLICATION_CONTEXT ( 'configuration controlled 3d designs of mechanical parts and assemblies' ) ;
#39537=ORIENTED_EDGE ( 'NONE', *, *, #80201, .T. ) ;
#39616=PLANE ( 'NONE',  #4360 ) ;
#39755=FACE_OUTER_BOUND ( 'NONE', #37060, .T. ) ;
#40300=LINE ( 'NONE', #71251, #90562 ) ;
#40312=DIRECTION ( 'NONE',  ( 0.8246584009594635223, 0.5656310827093757876, 2.309263891220325920E-14 ) ) ;
#40420=ORIENTED_EDGE ( 'NONE', *, *, #15180, .T. ) ;
#40499=AXIS2_PLACEMENT_3D ( 'NONE', #64692, #26094, #86492 ) ;
#40699=EDGE_LOOP ( 'NONE', ( #80530, #85924, #1017, #4872 ) ) ;
#40872=ORIENTED_EDGE ( 'NONE', *, *, #42483, .T. ) ;
#41219=CARTESIAN_POINT ( 'NONE',  ( -15.87499999999997868, 0.000000000000000000, 0.000000000000000000 ) ) ;
#41343=ORIENTED_EDGE ( 'NONE', *, *, #71817, .T. ) ;
#41350=FACE_OUTER_BOUND ( 'NONE', #51174, .T. ) ;
#41539=ADVANCED_FACE ( 'NONE', ( #16549 ), #8952, .F. ) ;
#41674=CARTESIAN_POINT ( 'NONE',  ( 0.1645010273463760886, -0.3687607960183646449, -1.417169167140628350 ) ) ;
#41917=CARTESIAN_POINT ( 'NONE',  ( 2.100208336950355914, 1.530808498934186394E-16, -1.249999999999996003 ) ) ;
#41972=LINE ( 'NONE', #28223, #33139 ) ;
#42047=AXIS2_PLACEMENT_3D ( 'NONE', #12976, #19594, #42462 ) ;
#42309=ORIENTED_EDGE ( 'NONE', *, *, #44779, .F. ) ;
#42359=CARTESIAN_POINT ( 'NONE',  ( 13.60020833695035947, 0.000000000000000000, 1.249999999999999112 ) ) ;
#42462=DIRECTION ( 'NONE',  ( 0.8246584009594635223, 1.154631945610162960E-14, -0.5656310827093757876 ) ) ;
#42483=EDGE_CURVE ( 'NONE', #99053, #15989, #70195, .T. ) ;
#42576=PRODUCT ( 'oval head_am_B18.6.7M - M2.5 x 0.45 x 13 Type I Cross Recessed OHMS --13C', 'oval head_am_B18.6.7M - M2.5 x 0.45 x 13 Type I Cross Recessed OHMS --13C', '', ( #13540 ) ) ;
#42642=DIRECTION ( 'NONE',  ( 0.5656310827093757876, 2.995395837334948684E-15, -0.8246584009594636333 ) ) ;
#42686=LINE ( 'NONE', #74605, #8857 ) ;
#42974=ORIENTED_EDGE ( 'NONE', *, *, #49168, .F. ) ;
#43169=CARTESIAN_POINT ( 'NONE',  ( 0.02224039135773590858, -0.3828044741864804479, 0.3828044741864790601 ) ) ;
#43212=DIRECTION ( 'NONE',  ( 0.9951627101165076983, 0.000000000000000000, 0.09824042138329622254 ) ) ;
#43350=AXIS2_PLACEMENT_3D ( 'NONE', #37831, #53575, #47948 ) ;
#43643=DIRECTION ( 'NONE',  ( -0.8246584009594635223, 0.5656310827093757876, 1.065814103640150279E-14 ) ) ;
#43673=DIRECTION ( 'NONE',  ( -1.000000000000000000, -0.000000000000000000, -0.000000000000000000 ) ) ;
#43837=AXIS2_PLACEMENT_3D ( 'NONE', #4865, #43927, #22064 ) ;
#43927=DIRECTION ( 'NONE',  ( -0.09824042138329623641, -2.980407940728110405E-17, 0.9951627101165078093 ) ) ;
#43951=PLANE ( 'NONE',  #74123 ) ;
#44075=CARTESIAN_POINT ( 'NONE',  ( 0.000000000000000000, 0.3849999999999945688, 1.530000000000001359 ) ) ;
#44134=DIRECTION ( 'NONE',  ( 0.000000000000000000, 0.000000000000000000, 1.000000000000000000 ) ) ;
#44167=EDGE_CURVE ( 'NONE', #78612, #56245, #10201, .T. ) ;
#44284=ADVANCED_FACE ( 'NONE', ( #9194 ), #47270, .T. ) ;
#44357=AXIS2_PLACEMENT_3D ( 'NONE', #45862, #6295, #6786 ) ;
#44369=EDGE_LOOP ( 'NONE', ( #56078, #86192, #81311 ) ) ;
#44433=FACE_OUTER_BOUND ( 'NONE', #59412, .T. ) ;
#44455=ORIENTED_EDGE ( 'NONE', *, *, #76805, .T. ) ;
#44732=ORIENTED_EDGE ( 'NONE', *, *, #75809, .F. ) ;
#44760=VECTOR ( 'NONE', #82690, 1000.000000000000227 ) ;
#44779=EDGE_CURVE ( 'NONE', #56245, #31023, #91242, .T. ) ;
#44854=DIRECTION ( 'NONE',  ( 0.8219392559241307517, -0.5637660281018076480, -0.08114015731558694988 ) ) ;
#45159=ADVANCED_FACE ( 'NONE', ( #94062 ), #47904, .F. ) ;
#45256=DIRECTION ( 'NONE',  ( -1.000000000000000000, -0.000000000000000000, -0.000000000000000000 ) ) ;
#45312=CARTESIAN_POINT ( 'NONE',  ( 1.949999999999999734, 0.1924999999999993938, 0.1925000000000007261 ) ) ;
#45384=DIRECTION ( 'NONE',  ( -0.9951627101165078093, -0.09824042138329590335, -1.421085471520200214E-14 ) ) ;
#45604=EDGE_CURVE ( 'NONE', #20296, #74207, #96175, .T. ) ;
#45862=CARTESIAN_POINT ( 'NONE',  ( 2.230654205607476737, -0.1647943925233645579, -7.922169807384186089E-16 ) ) ;
#45920=EDGE_CURVE ( 'NONE', #23547, #64340, #47063, .T. ) ;
#45947=ORIENTED_EDGE ( 'NONE', *, *, #14342, .F. ) ;
#45960=CARTESIAN_POINT ( 'NONE',  ( 0.02224039135773590858, 0.3828044741864812250, -0.3828044741864797817 ) ) ;
#45993=ORIENTED_EDGE ( 'NONE', *, *, #66868, .F. ) ;
#46081=DIRECTION ( 'NONE',  ( 0.8219392559241306406, -0.08114015731558522904, -0.5637660281018079811 ) ) ;
#46376=CARTESIAN_POINT ( 'NONE',  ( 1.000208336950358934, 0.000000000000000000, 2.349999999999999645 ) ) ;
#46567=VECTOR ( 'NONE', #44854, 999.9999999999998863 ) ;
#46608=AXIS2_PLACEMENT_3D ( 'NONE', #87989, #78851, #40312 ) ;
#46696=ORIENTED_EDGE ( 'NONE', *, *, #17339, .F. ) ;
#46814=ORIENTED_EDGE ( 'NONE', *, *, #84842, .F. ) ;
#46972=ORIENTED_EDGE ( 'NONE', *, *, #25636, .F. ) ;
#47063=LINE ( 'NONE', #83600, #24885 ) ;
#47217=VECTOR ( 'NONE', #37881, 1000.000000000000114 ) ;
#47270=PLANE ( 'NONE',  #92826 ) ;
#47385=PLANE ( 'NONE',  #6660 ) ;
#47398=CYLINDRICAL_SURFACE ( 'NONE', #63040, 1.249999999999997558 ) ;
#47742=DIRECTION ( 'NONE',  ( 0.9951627101165076983, -0.09824042138329622254, -3.430045979798646929E-16 ) ) ;
#47751=DIRECTION ( 'NONE',  ( -1.000000000000000000, -0.000000000000000000, -0.000000000000000000 ) ) ;
#47885=DIRECTION ( 'NONE',  ( 0.9951627101165076983, -0.09824042138329622254, -3.430045979798646929E-16 ) ) ;
#47903=CARTESIAN_POINT ( 'NONE',  ( 13.60020833695035947, 0.000000000000000000, 0.000000000000000000 ) ) ;
#47904=PLANE ( 'NONE',  #50771 ) ;
#47948=DIRECTION ( 'NONE',  ( -0.9951627101165078093, 0.000000000000000000, 0.09824042138329590335 ) ) ;
#48038=CARTESIAN_POINT ( 'NONE',  ( 0.4325450954222598288, 2.877919977996279827E-16, -2.350000000000000089 ) ) ;
#48159=EDGE_LOOP ( 'NONE', ( #54681, #16222, #82183, #65211, #65532, #97602, #11525, #40872, #91863, #30873, #45993 ) ) ;
#48647=SHAPE_REPRESENTATION_RELATIONSHIP ( 'NONE' , 'NONE' ,  #32845, #59836 ) ;
#48752=CARTESIAN_POINT ( 'NONE',  ( 2.230654205607476293, 0.1647943925233646134, -7.514475724998474108E-17 ) ) ;
#48778=ORIENTED_EDGE ( 'NONE', *, *, #60912, .F. ) ;
#48826=ORIENTED_EDGE ( 'NONE', *, *, #64247, .T. ) ;
#49042=DIRECTION ( 'NONE',  ( 0.8246584009594636333, 0.5656310827093757876, 0.000000000000000000 ) ) ;
#49153=AXIS2_PLACEMENT_3D ( 'NONE', #91278, #36488, #21749 ) ;
#49168=EDGE_CURVE ( 'NONE', #78009, #95252, #76281, .T. ) ;
#49192=CARTESIAN_POINT ( 'NONE',  ( 6.573941812937369455, -7.905506363763796338E-18, 0.2639660507643297183 ) ) ;
#49267=FACE_OUTER_BOUND ( 'NONE', #59866, .T. ) ;
#49301=CARTESIAN_POINT ( 'NONE',  ( 2.230654205607476737, -2.168404344971008868E-16, 0.1647943925233645579 ) ) ;
#49472=EDGE_LOOP ( 'NONE', ( #1738, #64280, #18138, #96597 ) ) ;
#49783=CIRCLE ( 'NONE', #90250, 6.119803529381341534 ) ;
#49919=LINE ( 'NONE', #80850, #33360 ) ;
#50131=( LENGTH_UNIT ( ) NAMED_UNIT ( * ) SI_UNIT ( .MILLI., .METRE. ) );
#50190=DIRECTION ( 'NONE',  ( 0.8219392559241307517, 0.5637660281018075370, 0.08114015731558725519 ) ) ;
#50280=AXIS2_PLACEMENT_3D ( 'NONE', #88884, #12231, #43212 ) ;
#50367=CARTESIAN_POINT ( 'NONE',  ( 2.100208336950355914, 0.000000000000000000, 1.249999999999996003 ) ) ;
#50498=EDGE_LOOP ( 'NONE', ( #15903, #94486, #80415 ) ) ;
#50511=LINE ( 'NONE', #41917, #21395 ) ;
#50771=AXIS2_PLACEMENT_3D ( 'NONE', #715, #31664, #31162 ) ;
#51174=EDGE_LOOP ( 'NONE', ( #58205, #64185, #94069, #29016, #48778 ) ) ;
#51290=EDGE_CURVE ( 'NONE', #88013, #54552, #41972, .T. ) ;
#51304=CIRCLE ( 'NONE', #2717, 1.249999999999996003 ) ;
#51722=VECTOR ( 'NONE', #56675, 1000.000000000000000 ) ;
#51961=CARTESIAN_POINT ( 'NONE',  ( -15.87499999999997868, 0.000000000000000000, 0.000000000000000000 ) ) ;
#52109=ORIENTED_EDGE ( 'NONE', *, *, #87146, .F. ) ;
#52228=LINE ( 'NONE', #92271, #14634 ) ;
#52237=VECTOR ( 'NONE', #13269, 1000.000000000000227 ) ;
#52381=DIRECTION ( 'NONE',  ( 0.000000000000000000, -1.000000000000000000, -1.224646799147353207E-16 ) ) ;
#52566=FACE_OUTER_BOUND ( 'NONE', #69651, .T. ) ;
#52970=DIRECTION ( 'NONE',  ( -1.000000000000000000, -0.000000000000000000, -0.000000000000000000 ) ) ;
#53054=CIRCLE ( 'NONE', #43350, 6.594667762285749468 ) ;
#53116=ADVANCED_FACE ( 'NONE', ( #41350 ), #72304, .T. ) ;
#53409=ORIENTED_EDGE ( 'NONE', *, *, #75809, .T. ) ;
#53575=DIRECTION ( 'NONE',  ( 0.09824042138329590335, -4.470611911092166224E-17, 0.9951627101165079203 ) ) ;
#53932=VERTEX_POINT ( 'NONE', #68456 ) ;
#53992=CARTESIAN_POINT ( 'NONE',  ( 6.573941812937369455, 1.185825954564562440E-17, -0.2639660507643281639 ) ) ;
#54552=VERTEX_POINT ( 'NONE', #25018 ) ;
#54636=CIRCLE ( 'NONE', #59483, 1.249999999999996003 ) ;
#54681=ORIENTED_EDGE ( 'NONE', *, *, #17578, .T. ) ;
#54844=DIRECTION ( 'NONE',  ( -1.000000000000000000, -0.000000000000000000, -0.000000000000000000 ) ) ;
#55163=DIRECTION ( 'NONE',  ( 0.09824042138329625029, 0.9951627101165079203, 3.504396110891627214E-15 ) ) ;
#55397=LINE ( 'NONE', #86334, #61325 ) ;
#55744=CARTESIAN_POINT ( 'NONE',  ( 1.000208336950358934, 0.000000000000000000, 0.000000000000000000 ) ) ;
#55862=EDGE_CURVE ( 'NONE', #95252, #20296, #50511, .T. ) ;
#56024=DIRECTION ( 'NONE',  ( -1.000000000000000000, -0.000000000000000000, -0.000000000000000000 ) ) ;
#56078=ORIENTED_EDGE ( 'NONE', *, *, #64247, .F. ) ;
#56245=VERTEX_POINT ( 'NONE', #36034 ) ;
#56538=CIRCLE ( 'NONE', #67839, 6.594667762285751245 ) ;
#56675=DIRECTION ( 'NONE',  ( 0.000000000000000000, 1.000000000000000000, 0.000000000000000000 ) ) ;
#57020=ADVANCED_FACE ( 'NONE', ( #80974 ), #89587, .F. ) ;
#57309=DIRECTION ( 'NONE',  ( 0.09824042138329625029, 2.980407940728111021E-17, -0.9951627101165079203 ) ) ;
#57442=VERTEX_POINT ( 'NONE', #6162 ) ;
#57528=DIRECTION ( 'NONE',  ( 0.000000000000000000, 1.408054769461693696E-16, -1.000000000000000000 ) ) ;
#57908=EDGE_LOOP ( 'NONE', ( #42974, #78541, #9810, #68928 ) ) ;
#58160=CARTESIAN_POINT ( 'NONE',  ( 0.1645010273463769490, 0.3687607960183755251, -1.417169167140624575 ) ) ;
#58205=ORIENTED_EDGE ( 'NONE', *, *, #80201, .F. ) ;
#58208=AXIS2_PLACEMENT_3D ( 'NONE', #96838, #26335, #12093 ) ;
#58451=CYLINDRICAL_SURFACE ( 'NONE', #9185, 2.349999999999999645 ) ;
#58903=CARTESIAN_POINT ( 'NONE',  ( 0.4325450954222598288, 0.000000000000000000, 0.000000000000000000 ) ) ;
#59395=LINE ( 'NONE', #14201, #80278 ) ;
#59412=EDGE_LOOP ( 'NONE', ( #67635, #63147, #3324 ) ) ;
#59483=AXIS2_PLACEMENT_3D ( 'NONE', #92150, #93646, #23126 ) ;
#59562=CIRCLE ( 'NONE', #74117, 1.249999999999999112 ) ;
#59836=ADVANCED_BREP_SHAPE_REPRESENTATION ( '', ( #76408, #37391 ), #82851 ) ;
#59866=EDGE_LOOP ( 'NONE', ( #71612, #11183, #15860, #28739 ) ) ;
#60007=DIRECTION ( 'NONE',  ( 0.000000000000000000, -1.224646799147353207E-16, 1.000000000000000000 ) ) ;
#60235=DIRECTION ( 'NONE',  ( 0.000000000000000000, 0.000000000000000000, 1.000000000000000000 ) ) ;
#60541=AXIS2_PLACEMENT_3D ( 'NONE', #55744, #25268, #71964 ) ;
#60588=LINE ( 'NONE', #29112, #46567 ) ;
#60731=SPHERICAL_SURFACE ( 'NONE', #84670, 6.600000000000001421 ) ;
#60815=AXIS2_PLACEMENT_3D ( 'NONE', #17556, #65266, #27176 ) ;
#60830=AXIS2_PLACEMENT_3D ( 'NONE', #15468, #69773, #250 ) ;
#60912=EDGE_CURVE ( 'NONE', #16787, #4203, #30297, .T. ) ;
#61236=CARTESIAN_POINT ( 'NONE',  ( 0.000000000000000000, -1.530000000000000027, 0.3849999999999990652 ) ) ;
#61325=VECTOR ( 'NONE', #25433, 1000.000000000000227 ) ;
#61487=CARTESIAN_POINT ( 'NONE',  ( 2.100208336950355914, 0.000000000000000000, 0.000000000000000000 ) ) ;
#61781=ORIENTED_EDGE ( 'NONE', *, *, #8875, .F. ) ;
#62723=VERTEX_POINT ( 'NONE', #50367 ) ;
#63040=AXIS2_PLACEMENT_3D ( 'NONE', #76818, #85441, #85952 ) ;
#63147=ORIENTED_EDGE ( 'NONE', *, *, #51290, .T. ) ;
#63447=DIRECTION ( 'NONE',  ( 0.000000000000000000, 0.000000000000000000, 1.000000000000000000 ) ) ;
#63695=AXIS2_PLACEMENT_3D ( 'NONE', #33662, #85065, #38394 ) ;
#63698=EDGE_LOOP ( 'NONE', ( #52109, #46814 ) ) ;
#64185=ORIENTED_EDGE ( 'NONE', *, *, #45604, .T. ) ;
#64247=EDGE_CURVE ( 'NONE', #76987, #4757, #55397, .T. ) ;
#64280=ORIENTED_EDGE ( 'NONE', *, *, #84067, .T. ) ;
#64340=VERTEX_POINT ( 'NONE', #89835 ) ;
#64692=CARTESIAN_POINT ( 'NONE',  ( 6.573941812937369455, -7.905506363763796338E-18, 0.2639660507643297183 ) ) ;
#65178=EDGE_CURVE ( 'NONE', #91571, #88013, #56538, .T. ) ;
#65184=ADVANCED_FACE ( 'NONE', ( #31303 ), #6242, .T. ) ;
#65211=ORIENTED_EDGE ( 'NONE', *, *, #29767, .F. ) ;
#65266=DIRECTION ( 'NONE',  ( -1.000000000000000000, -0.000000000000000000, -0.000000000000000000 ) ) ;
#65438=CARTESIAN_POINT ( 'NONE',  ( 0.000000000000000000, -1.530000000000000027, -0.3850000000000000089 ) ) ;
#65490=DIRECTION ( 'NONE',  ( 0.8246584009594636333, -1.974890369949422146E-15, 0.5656310827093757876 ) ) ;
#65521=EDGE_CURVE ( 'NONE', #91571, #54552, #40300, .T. ) ;
#65532=ORIENTED_EDGE ( 'NONE', *, *, #76562, .T. ) ;
#65892=EDGE_CURVE ( 'NONE', #4551, #11386, #24135, .T. ) ;
#65957=EDGE_CURVE ( 'NONE', #88013, #31023, #80861, .T. ) ;
#66084=AXIS2_PLACEMENT_3D ( 'NONE', #82194, #12679, #43643 ) ;
#66300=EDGE_LOOP ( 'NONE', ( #84240, #79129, #96385, #46696 ) ) ;
#66509=LINE ( 'NONE', #27913, #44760 ) ;
#66851=LINE ( 'NONE', #97772, #90263 ) ;
#66868=EDGE_CURVE ( 'NONE', #4203, #53932, #80226, .T. ) ;
#66930=AXIS2_PLACEMENT_3D ( 'NONE', #29029, #60007, #52381 ) ;
#66953=EDGE_LOOP ( 'NONE', ( #91838, #15253, #85062, #20373 ) ) ;
#67635=ORIENTED_EDGE ( 'NONE', *, *, #65957, .F. ) ;
#67766=EDGE_CURVE ( 'NONE', #23547, #54552, #49919, .T. ) ;
#67839=AXIS2_PLACEMENT_3D ( 'NONE', #23679, #55163, #17077 ) ;
#68010=DIRECTION ( 'NONE',  ( -0.7071067811865452413, 0.000000000000000000, 0.7071067811865497932 ) ) ;
#68384=LINE ( 'NONE', #29811, #51722 ) ;
#68456=CARTESIAN_POINT ( 'NONE',  ( 0.1553305729023591875, -1.423459158329792640, 2.407412430484044816E-32 ) ) ;
#68457=AXIS2_PLACEMENT_3D ( 'NONE', #53992, #84920, #15404 ) ;
#68884=DIRECTION ( 'NONE',  ( 0.000000000000000000, -1.000000000000000000, -2.816109538923387391E-16 ) ) ;
#68928=ORIENTED_EDGE ( 'NONE', *, *, #84145, .F. ) ;
#69047=CIRCLE ( 'NONE', #22022, 2.350000000000000089 ) ;
#69091=DIRECTION ( 'NONE',  ( -1.000000000000000000, 0.000000000000000000, 0.000000000000000000 ) ) ;
#69324=DIRECTION ( 'NONE',  ( -0.09824042138329590335, 0.9951627101165078093, 3.519298150595267489E-15 ) ) ;
#69651=EDGE_LOOP ( 'NONE', ( #10285, #26483, #44455, #84303, #46972 ) ) ;
#69773=DIRECTION ( 'NONE',  ( 0.000000000000000000, 0.000000000000000000, -1.000000000000000000 ) ) ;
#70001=EDGE_CURVE ( 'NONE', #99053, #11386, #29044, .T. ) ;
#70080=DIRECTION ( 'NONE',  ( 0.09824042138329590335, -0.9951627101165079203, -3.519298150595267883E-15 ) ) ;
#70094=ORIENTED_EDGE ( 'NONE', *, *, #60912, .T. ) ;
#70195=CIRCLE ( 'NONE', #83150, 6.594667762285749468 ) ;
#70601=CARTESIAN_POINT ( 'NONE',  ( 1.949999999999999956, 0.1925000000000000044, -0.1925000000000000600 ) ) ;
#70931=ORIENTED_EDGE ( 'NONE', *, *, #66868, .T. ) ;
#71080=FACE_OUTER_BOUND ( 'NONE', #94017, .T. ) ;
#71088=DIRECTION ( 'NONE',  ( 0.000000000000000000, 0.000000000000000000, 1.000000000000000000 ) ) ;
#71251=CARTESIAN_POINT ( 'NONE',  ( 0.000000000000000000, 0.3850000000000053935, -1.529999999999998916 ) ) ;
#71514=DIRECTION ( 'NONE',  ( 0.000000000000000000, 0.000000000000000000, 1.000000000000000000 ) ) ;
#71612=ORIENTED_EDGE ( 'NONE', *, *, #87146, .T. ) ;
#71817=EDGE_CURVE ( 'NONE', #99053, #64340, #52228, .T. ) ;
#71875=AXIS2_PLACEMENT_3D ( 'NONE', #1353, #32288, #17060 ) ;
#71964=DIRECTION ( 'NONE',  ( 0.000000000000000000, 0.000000000000000000, 1.000000000000000000 ) ) ;
#72304=CYLINDRICAL_SURFACE ( 'NONE', #4108, 2.349999999999999645 ) ;
#72538=ORIENTED_EDGE ( 'NONE', *, *, #65892, .F. ) ;
#73412=DIRECTION ( 'NONE',  ( 0.9903949459893286456, -0.09776975748869043414, 0.09776975748869007332 ) ) ;
#73950=DIRECTION ( 'NONE',  ( 0.000000000000000000, -1.408054769461694189E-16, 1.000000000000000000 ) ) ;
#74117=AXIS2_PLACEMENT_3D ( 'NONE', #28393, #37512, #44134 ) ;
#74123=AXIS2_PLACEMENT_3D ( 'NONE', #97734, #29720, #5881 ) ;
#74206=ADVANCED_FACE ( 'NONE', ( #39755 ), #47385, .T. ) ;
#74207=VERTEX_POINT ( 'NONE', #46376 ) ;
#74398=VECTOR ( 'NONE', #46081, 1000.000000000000000 ) ;
#74605=CARTESIAN_POINT ( 'NONE',  ( 2.100208336950355914, 0.000000000000000000, 1.249999999999996003 ) ) ;
#74611=DIRECTION ( 'NONE',  ( 0.000000000000000000, 0.000000000000000000, 1.000000000000000000 ) ) ;
#75727=AXIS2_PLACEMENT_3D ( 'NONE', #85041, #69324, #86547 ) ;
#75797=PLANE ( 'NONE',  #44357 ) ;
#75809=EDGE_CURVE ( 'NONE', #23547, #4551, #82788, .T. ) ;
#75902=CARTESIAN_POINT ( 'NONE',  ( 0.4325450954222598288, 0.000000000000000000, 0.000000000000000000 ) ) ;
#76239=ADVANCED_FACE ( 'NONE', ( #100244 ), #60731, .T. ) ;
#76281=LINE ( 'NONE', #23479, #8669 ) ;
#76408=MANIFOLD_SOLID_BREP ( 'CirPattern1', #1506 ) ;
#76562=EDGE_CURVE ( 'NONE', #95664, #4551, #11725, .T. ) ;
#76775=CARTESIAN_POINT ( 'NONE',  ( 5.202077965628057576, 2.038091937962834166, 2.869745073849996442E-16 ) ) ;
#76805=EDGE_CURVE ( 'NONE', #31023, #54552, #82802, .T. ) ;
#76818=CARTESIAN_POINT ( 'NONE',  ( -15.87499999999997868, 0.000000000000000000, 0.000000000000000000 ) ) ;
#76987=VERTEX_POINT ( 'NONE', #35035 ) ;
#77027=ORIENTED_EDGE ( 'NONE', *, *, #10382, .F. ) ;
#77151=LINE ( 'NONE', #24379, #98740 ) ;
#77619=ADVANCED_FACE ( 'NONE', ( #5451 ), #23151, .T. ) ;
#78009=VERTEX_POINT ( 'NONE', #9195 ) ;
#78143=VERTEX_POINT ( 'NONE', #41674 ) ;
#78541=ORIENTED_EDGE ( 'NONE', *, *, #84842, .T. ) ;
#78612=VERTEX_POINT ( 'NONE', #12070 ) ;
#78762=VERTEX_POINT ( 'NONE', #7454 ) ;
#78851=DIRECTION ( 'NONE',  ( -0.5656310827093756766, 0.8246584009594636333, 1.161164194647626880E-16 ) ) ;
#78970=DIRECTION ( 'NONE',  ( -1.000000000000000000, -0.000000000000000000, -0.000000000000000000 ) ) ;
#79129=ORIENTED_EDGE ( 'NONE', *, *, #55862, .T. ) ;
#79635=ORIENTED_EDGE ( 'NONE', *, *, #93039, .T. ) ;
#79659=CARTESIAN_POINT ( 'NONE',  ( 2.230654205607476737, -2.168404344971008868E-16, 0.1647943925233645579 ) ) ;
#79677=PRODUCT_DEFINITION_FORMATION_WITH_SPECIFIED_SOURCE ( 'ANY', '', #42576, .NOT_KNOWN. ) ;
#79773=AXIS2_PLACEMENT_3D ( 'NONE', #38488, #1937, #23748 ) ;
#79835=DIRECTION ( 'NONE',  ( 0.000000000000000000, 0.000000000000000000, 1.000000000000000000 ) ) ;
#79856=DIRECTION ( 'NONE',  ( 0.09824042138329590335, -0.9951627101165079203, -3.519298150595267883E-15 ) ) ;
#80194=CARTESIAN_POINT ( 'NONE',  ( -15.87499999999997868, 0.000000000000000000, 0.000000000000000000 ) ) ;
#80201=EDGE_CURVE ( 'NONE', #20296, #16787, #77151, .T. ) ;
#80226=CIRCLE ( 'NONE', #60830, 6.600000000000001421 ) ;
#80230=DIRECTION ( 'NONE',  ( -0.09824042138329590335, 4.470611911092166224E-17, -0.9951627101165078093 ) ) ;
#80278=VECTOR ( 'NONE', #82225, 1000.000000000000000 ) ;
#80415=ORIENTED_EDGE ( 'NONE', *, *, #30402, .F. ) ;
#80530=ORIENTED_EDGE ( 'NONE', *, *, #70001, .T. ) ;
#80619=PRODUCT_DEFINITION_SHAPE ( 'NONE', 'NONE',  #3602 ) ;
#80850=CARTESIAN_POINT ( 'NONE',  ( 1.949999999999999956, 0.1924999999999999489, 0.1925000000000000044 ) ) ;
#80861=CIRCLE ( 'NONE', #85714, 6.594667762285751245 ) ;
#80974=FACE_OUTER_BOUND ( 'NONE', #92820, .T. ) ;
#81258=FACE_OUTER_BOUND ( 'NONE', #27937, .T. ) ;
#81309=AXIS2_PLACEMENT_3D ( 'NONE', #79659, #10159, #37986 ) ;
#81311=ORIENTED_EDGE ( 'NONE', *, *, #98676, .F. ) ;
#81559=FACE_OUTER_BOUND ( 'NONE', #44369, .T. ) ;
#82183=ORIENTED_EDGE ( 'NONE', *, *, #44167, .T. ) ;
#82194=CARTESIAN_POINT ( 'NONE',  ( 5.202077965628057576, -2.038091937962834166, -2.869745073849994963E-16 ) ) ;
#82225=DIRECTION ( 'NONE',  ( -1.000000000000000000, -0.000000000000000000, -0.000000000000000000 ) ) ;
#82690=DIRECTION ( 'NONE',  ( 0.9903949459893287566, 0.09776975748869010108, -0.09776975748868974025 ) ) ;
#82788=LINE ( 'NONE', #7159, #52237 ) ;
#82802=LINE ( 'NONE', #90922, #92777 ) ;
#82851=( GEOMETRIC_REPRESENTATION_CONTEXT ( 3 ) GLOBAL_UNCERTAINTY_ASSIGNED_CONTEXT ( ( #20554 ) ) GLOBAL_UNIT_ASSIGNED_CONTEXT ( ( #50131, #26288, #89190 ) ) REPRESENTATION_CONTEXT ( 'NONE', 'WORKASPACE' ) );
#82957=CIRCLE ( 'NONE', #79773, 2.350000000000000089 ) ;
#83150=AXIS2_PLACEMENT_3D ( 'NONE', #20520, #70080, #45384 ) ;
#83312=ORIENTED_EDGE ( 'NONE', *, *, #28012, .T. ) ;
#83600=CARTESIAN_POINT ( 'NONE',  ( 1.949999999999999956, 0.1924999999999999489, 0.1925000000000000044 ) ) ;
#84040=AXIS2_PLACEMENT_3D ( 'NONE', #32808, #78970, #16569 ) ;
#84048=DIRECTION ( 'NONE',  ( 0.000000000000000000, -1.000000000000000000, 0.000000000000000000 ) ) ;
#84067=EDGE_CURVE ( 'NONE', #76987, #64340, #66851, .T. ) ;
#84145=EDGE_CURVE ( 'NONE', #95252, #62723, #54636, .T. ) ;
#84240=ORIENTED_EDGE ( 'NONE', *, *, #18647, .T. ) ;
#84303=ORIENTED_EDGE ( 'NONE', *, *, #67766, .F. ) ;
#84626=LINE ( 'NONE', #44075, #74398 ) ;
#84670=AXIS2_PLACEMENT_3D ( 'NONE', #91654, #60235, #84048 ) ;
#84842=EDGE_CURVE ( 'NONE', #78009, #5411, #59562, .T. ) ;
#84881=ORIENTED_EDGE ( 'NONE', *, *, #87524, .F. ) ;
#84920=DIRECTION ( 'NONE',  ( 0.09824042138329590335, -4.470611911092166224E-17, 0.9951627101165079203 ) ) ;
#85041=CARTESIAN_POINT ( 'NONE',  ( 2.230654205607476737, -0.1647943925233645579, -7.922169807384186089E-16 ) ) ;
#85062=ORIENTED_EDGE ( 'NONE', *, *, #3191, .T. ) ;
#85065=DIRECTION ( 'NONE',  ( 0.000000000000000000, 0.000000000000000000, 1.000000000000000000 ) ) ;
#85300=EDGE_CURVE ( 'NONE', #78143, #76987, #6938, .T. ) ;
#85441=DIRECTION ( 'NONE',  ( -1.000000000000000000, -0.000000000000000000, -0.000000000000000000 ) ) ;
#85714=AXIS2_PLACEMENT_3D ( 'NONE', #49192, #57309, #97342 ) ;
#85924=ORIENTED_EDGE ( 'NONE', *, *, #87524, .T. ) ;
#85952=DIRECTION ( 'NONE',  ( 0.000000000000000000, 0.000000000000000000, 1.000000000000000000 ) ) ;
#86192=ORIENTED_EDGE ( 'NONE', *, *, #85300, .F. ) ;
#86334=CARTESIAN_POINT ( 'NONE',  ( 2.246611357655419638, -0.1632191352058106892, -0.1632191352058112721 ) ) ;
#86492=DIRECTION ( 'NONE',  ( 0.9951627101165076983, 0.000000000000000000, 0.09824042138329622254 ) ) ;
#86547=DIRECTION ( 'NONE',  ( -0.9951627101165076983, -0.09824042138329588947, -3.430045979798635096E-16 ) ) ;
#86789=DIRECTION ( 'NONE',  ( -0.09824042138329623641, -0.9951627101165078093, -3.504396110891626425E-15 ) ) ;
#87146=EDGE_CURVE ( 'NONE', #5411, #78009, #17687, .T. ) ;
#87445=APPLICATION_CONTEXT ( 'configuration controlled 3d designs of mechanical parts and assemblies' ) ;
#87524=EDGE_CURVE ( 'NONE', #11386, #23547, #84626, .T. ) ;
#87849=FACE_OUTER_BOUND ( 'NONE', #21594, .T. ) ;
#87989=CARTESIAN_POINT ( 'NONE',  ( 5.202077965628057576, 2.038091937962834166, 2.869745073849996442E-16 ) ) ;
#88013=VERTEX_POINT ( 'NONE', #45960 ) ;
#88617=CARTESIAN_POINT ( 'NONE',  ( 0.4325450954222598288, -2.349999999999997868, 0.000000000000000000 ) ) ;
#88793=FACE_OUTER_BOUND ( 'NONE', #50498, .T. ) ;
#88884=CARTESIAN_POINT ( 'NONE',  ( 2.230654205607476293, -6.505213034913026604E-16, -0.1647943925233646134 ) ) ;
#88901=ORIENTED_EDGE ( 'NONE', *, *, #20794, .F. ) ;
#89190=( NAMED_UNIT ( * ) SI_UNIT ( $, .STERADIAN. ) SOLID_ANGLE_UNIT ( ) );
#89587=PLANE ( 'NONE',  #36679 ) ;
#89835=CARTESIAN_POINT ( 'NONE',  ( 1.949999999999999956, -0.1925000000000001710, 0.1924999999999999212 ) ) ;
#90250=AXIS2_PLACEMENT_3D ( 'NONE', #76775, #22493, #39231 ) ;
#90263=VECTOR ( 'NONE', #73950, 1000.000000000000000 ) ;
#90562=VECTOR ( 'NONE', #15447, 1000.000000000000114 ) ;
#90646=ORIENTED_EDGE ( 'NONE', *, *, #17339, .T. ) ;
#90922=CARTESIAN_POINT ( 'NONE',  ( 0.000000000000000000, 1.530000000000000027, -0.3849999999999998979 ) ) ;
#91242=CIRCLE ( 'NONE', #11849, 6.119803529381342422 ) ;
#91278=CARTESIAN_POINT ( 'NONE',  ( 2.100208336950355914, 0.000000000000000000, 0.000000000000000000 ) ) ;
#91413=CARTESIAN_POINT ( 'NONE',  ( 0.1645010273463760886, 1.417169167140627462, -0.3687607960183705846 ) ) ;
#91571=VERTEX_POINT ( 'NONE', #58160 ) ;
#91654=CARTESIAN_POINT ( 'NONE',  ( 6.600000000000001421, 0.000000000000000000, 0.000000000000000000 ) ) ;
#91838=ORIENTED_EDGE ( 'NONE', *, *, #10382, .T. ) ;
#91863=ORIENTED_EDGE ( 'NONE', *, *, #21288, .T. ) ;
#91961=CARTESIAN_POINT ( 'NONE',  ( 0.1645010273463760886, -0.3687607960183749145, 1.417169167140625907 ) ) ;
#92150=CARTESIAN_POINT ( 'NONE',  ( 2.100208336950355914, 0.000000000000000000, 0.000000000000000000 ) ) ;
#92271=CARTESIAN_POINT ( 'NONE',  ( 0.000000000000000000, -0.3850000000000046163, 1.529999999999998916 ) ) ;
#92543=CARTESIAN_POINT ( 'NONE',  ( 2.230654205607476293, 0.1647943925233646134, -7.514475724998474108E-17 ) ) ;
#92664=CARTESIAN_POINT ( 'NONE',  ( 0.000000000000000000, -0.3849999999999936806, -1.530000000000001359 ) ) ;
#92777=VECTOR ( 'NONE', #15285, 1000.000000000000000 ) ;
#92820=EDGE_LOOP ( 'NONE', ( #2280, #83312, #18576, #17600, #88901 ) ) ;
#92826=AXIS2_PLACEMENT_3D ( 'NONE', #70601, #69091, #38641 ) ;
#92860=CONICAL_SURFACE ( 'NONE', #49153, 1.249999999999996003, 0.7853981633974514986 ) ;
#93039=EDGE_CURVE ( 'NONE', #78762, #4757, #27534, .T. ) ;
#93555=AXIS2_PLACEMENT_3D ( 'NONE', #96410, #42642, #65490 ) ;
#93646=DIRECTION ( 'NONE',  ( -1.000000000000000000, -0.000000000000000000, -0.000000000000000000 ) ) ;
#93754=ADVANCED_FACE ( 'NONE', ( #81258 ), #20340, .T. ) ;
#93908=CYLINDRICAL_SURFACE ( 'NONE', #23118, 1.249999999999997558 ) ;
#94017=EDGE_LOOP ( 'NONE', ( #37193, #31815, #95229 ) ) ;
#94062=FACE_OUTER_BOUND ( 'NONE', #40699, .T. ) ;
#94069=ORIENTED_EDGE ( 'NONE', *, *, #14342, .T. ) ;
#94411=AXIS2_PLACEMENT_3D ( 'NONE', #94912, #35024, #6930 ) ;
#94486=ORIENTED_EDGE ( 'NONE', *, *, #29709, .T. ) ;
#94912=CARTESIAN_POINT ( 'NONE',  ( 5.202077965628057576, -7.402934475628873363E-15, 2.038091937962834166 ) ) ;
#95025=ADVANCED_FACE ( 'NONE', ( #7823 ), #47398, .T. ) ;
#95229=ORIENTED_EDGE ( 'NONE', *, *, #65178, .F. ) ;
#95252=VERTEX_POINT ( 'NONE', #20923 ) ;
#95664=VERTEX_POINT ( 'NONE', #1863 ) ;
#95997=DIRECTION ( 'NONE',  ( -1.000000000000000000, -0.000000000000000000, -0.000000000000000000 ) ) ;
#96098=DIRECTION ( 'NONE',  ( -0.9951627101165078093, -0.09824042138329590335, 0.000000000000000000 ) ) ;
#96175=CIRCLE ( 'NONE', #60541, 2.349999999999999645 ) ;
#96385=ORIENTED_EDGE ( 'NONE', *, *, #15180, .F. ) ;
#96387=ORIENTED_EDGE ( 'NONE', *, *, #96566, .F. ) ;
#96410=CARTESIAN_POINT ( 'NONE',  ( 1.949999999999999956, 0.1925000000000007538, -0.1924999999999994493 ) ) ;
#96566=EDGE_CURVE ( 'NONE', #78612, #16787, #100376, .T. ) ;
#96597=ORIENTED_EDGE ( 'NONE', *, *, #67766, .T. ) ;
#96838=CARTESIAN_POINT ( 'NONE',  ( 6.573941812937369455, -0.2639660507643297183, -9.295380466955404257E-16 ) ) ;
#97063=AXIS2_PLACEMENT_3D ( 'NONE', #47903, #56024, #79835 ) ;
#97342=DIRECTION ( 'NONE',  ( 0.9951627101165076983, 0.000000000000000000, 0.09824042138329622254 ) ) ;
#97602=ORIENTED_EDGE ( 'NONE', *, *, #65892, .T. ) ;
#97734=CARTESIAN_POINT ( 'NONE',  ( 1.949999999999999956, 0.1924999999999999489, 0.1925000000000000322 ) ) ;
#97772=CARTESIAN_POINT ( 'NONE',  ( 1.949999999999999956, -0.1925000000000001155, -0.1925000000000000600 ) ) ;
#98229=VERTEX_POINT ( 'NONE', #4981 ) ;
#98548=ADVANCED_FACE ( 'NONE', ( #44433 ), #13459, .T. ) ;
#98640=ORIENTED_EDGE ( 'NONE', *, *, #25636, .T. ) ;
#98676=EDGE_CURVE ( 'NONE', #4757, #78143, #21079, .T. ) ;
#98740=VECTOR ( 'NONE', #54844, 1000.000000000000000 ) ;
#99053=VERTEX_POINT ( 'NONE', #91961 ) ;
#99657=DESIGN_CONTEXT ( 'detailed design', #87445, 'design' ) ;
#99923=CARTESIAN_POINT ( 'NONE',  ( 0.4325450954222598288, 0.000000000000000000, 0.000000000000000000 ) ) ;
#100244=FACE_OUTER_BOUND ( 'NONE', #19705, .T. ) ;
#100376=CIRCLE ( 'NONE', #3144, 2.350000000000000089 ) ;
#100462=COLOUR_RGB('Light Gray', 0.08235294, 0.09019608, 0.10196078);
#100463=FILL_AREA_STYLE_COLOUR('',#100462);
#100464=FILL_AREA_STYLE('',(#100463));
#100465=SURFACE_STYLE_FILL_AREA(#100464);
#100466=SURFACE_SIDE_STYLE('',(#100465));
#100467=SURFACE_STYLE_USAGE(.BOTH.,#100466);
#100468=PRESENTATION_STYLE_ASSIGNMENT((#100467));
#100492=STYLED_ITEM('',(#100468),#76408);
#100493=MECHANICAL_DESIGN_GEOMETRIC_PRESENTATION_REPRESENTATION('',(#100492),#82851);
ENDSEC;
END-ISO-10303-21;
